ISO-10303-21;
HEADER;
/* Generated by software containing ST-Developer
 * from STEP Tools, Inc. (www.steptools.com) 
 */

FILE_DESCRIPTION(
/* description */ ('Over-Centre Plunger Toggle Clamp on Slotted Fixture Frame'),
/* implementation_level */ '2;1');

FILE_NAME(
/* name */ 
'M4x30 stop screw.step',
/* time_stamp */ '2026-10-28T03:23:24-07:00',
/* author */ (''),
/* organization */ (''),
/* preprocessor_version */ 'ST-DEVELOPER v20.2',
/* originating_system */ 'Autodesk Translation Framework v15.17.0.0',
/* authorisation */ '');

FILE_SCHEMA (('AUTOMOTIVE_DESIGN { 1 0 10303 214 3 1 1 }'));
ENDSEC;

DATA;
#10=MECHANICAL_DESIGN_GEOMETRIC_PRESENTATION_REPRESENTATION('',(#544),#15212);
#398=ORIENTED_CLOSED_SHELL('',*,#8277,.F.);
#402=BREP_WITH_VOIDS('Body1',#8278,(#398));
#413=CONICAL_SURFACE('',#9367,0.325,0.785398163397448);
#414=CONICAL_SURFACE('',#9371,0.335,0.785398163397448);
#415=CONICAL_SURFACE('',#9375,0.21,0.463647609000806);
#416=CONICAL_SURFACE('',#9379,0.18,0.785398163397448);
#452=SHAPE_REPRESENTATION_RELATIONSHIP('SRR','None',#15428,#494);
#494=ADVANCED_BREP_SHAPE_REPRESENTATION('',(#402),#15190);
#544=STYLED_ITEM('',(#15726),#402);
#740=FACE_BOUND('',#2018,.T.);
#741=FACE_BOUND('',#2026,.T.);
#972=PLANE('',#9351);
#973=PLANE('',#9352);
#974=PLANE('',#9353);
#975=PLANE('',#9354);
#976=PLANE('',#9355);
#977=PLANE('',#9356);
#978=PLANE('',#9357);
#979=PLANE('',#9358);
#980=PLANE('',#9359);
#981=PLANE('',#9364);
#982=PLANE('',#9365);
#983=PLANE('',#9373);
#1394=FACE_OUTER_BOUND('',#2009,.T.);
#1395=FACE_OUTER_BOUND('',#2010,.T.);
#1396=FACE_OUTER_BOUND('',#2011,.T.);
#1397=FACE_OUTER_BOUND('',#2012,.T.);
#1398=FACE_OUTER_BOUND('',#2013,.T.);
#1399=FACE_OUTER_BOUND('',#2014,.T.);
#1400=FACE_OUTER_BOUND('',#2015,.T.);
#1401=FACE_OUTER_BOUND('',#2016,.T.);
#1402=FACE_OUTER_BOUND('',#2017,.T.);
#1403=FACE_OUTER_BOUND('',#2019,.T.);
#1404=FACE_OUTER_BOUND('',#2020,.T.);
#1405=FACE_OUTER_BOUND('',#2021,.T.);
#1406=FACE_OUTER_BOUND('',#2022,.T.);
#1407=FACE_OUTER_BOUND('',#2023,.T.);
#1408=FACE_OUTER_BOUND('',#2024,.T.);
#1409=FACE_OUTER_BOUND('',#2025,.T.);
#1410=FACE_OUTER_BOUND('',#2027,.T.);
#1411=FACE_OUTER_BOUND('',#2028,.T.);
#1412=FACE_OUTER_BOUND('',#2029,.T.);
#2009=EDGE_LOOP('',(#6937,#6938,#6939,#6940));
#2010=EDGE_LOOP('',(#6941,#6942,#6943,#6944));
#2011=EDGE_LOOP('',(#6945,#6946,#6947,#6948));
#2012=EDGE_LOOP('',(#6949,#6950,#6951,#6952));
#2013=EDGE_LOOP('',(#6953,#6954,#6955,#6956));
#2014=EDGE_LOOP('',(#6957,#6958,#6959,#6960));
#2015=EDGE_LOOP('',(#6961,#6962,#6963,#6964,#6965,#6966));
#2016=EDGE_LOOP('',(#6967,#6968,#6969,#6970,#6971,#6972));
#2017=EDGE_LOOP('',(#6973));
#2018=EDGE_LOOP('',(#6974));
#2019=EDGE_LOOP('',(#6975,#6976,#6977,#6978));
#2020=EDGE_LOOP('',(#6979));
#2021=EDGE_LOOP('',(#6980));
#2022=EDGE_LOOP('',(#6981,#6982,#6983,#6984));
#2023=EDGE_LOOP('',(#6985,#6986,#6987,#6988));
#2024=EDGE_LOOP('',(#6989,#6990,#6991,#6992));
#2025=EDGE_LOOP('',(#6993));
#2026=EDGE_LOOP('',(#6994));
#2027=EDGE_LOOP('',(#6995,#6996,#6997,#6998));
#2028=EDGE_LOOP('',(#6999,#7000,#7001,#7002));
#2029=EDGE_LOOP('',(#7003,#7004,#7005,#7006));
#2651=LINE('',#14197,#3281);
#2652=LINE('',#14199,#3282);
#2653=LINE('',#14201,#3283);
#2654=LINE('',#14202,#3284);
#2655=LINE('',#14205,#3285);
#2656=LINE('',#14207,#3286);
#2657=LINE('',#14208,#3287);
#2658=LINE('',#14211,#3288);
#2659=LINE('',#14213,#3289);
#2660=LINE('',#14214,#3290);
#2661=LINE('',#14217,#3291);
#2662=LINE('',#14219,#3292);
#2663=LINE('',#14220,#3293);
#2664=LINE('',#14223,#3294);
#2665=LINE('',#14225,#3295);
#2666=LINE('',#14226,#3296);
#2667=LINE('',#14228,#3297);
#2668=LINE('',#14229,#3298);
#2669=LINE('',#14239,#3299);
#2670=LINE('',#14248,#3300);
#2671=LINE('',#14252,#3301);
#2672=LINE('',#14256,#3302);
#2673=LINE('',#14263,#3303);
#2674=LINE('',#14267,#3304);
#2675=LINE('',#14269,#3305);
#3281=VECTOR('',#11352,1.);
#3282=VECTOR('',#11353,1.);
#3283=VECTOR('',#11354,1.);
#3284=VECTOR('',#11355,1.);
#3285=VECTOR('',#11358,1.);
#3286=VECTOR('',#11359,1.);
#3287=VECTOR('',#11360,1.);
#3288=VECTOR('',#11363,1.);
#3289=VECTOR('',#11364,1.);
#3290=VECTOR('',#11365,1.);
#3291=VECTOR('',#11368,1.);
#3292=VECTOR('',#11369,1.);
#3293=VECTOR('',#11370,1.);
#3294=VECTOR('',#11373,1.);
#3295=VECTOR('',#11374,1.);
#3296=VECTOR('',#11375,1.);
#3297=VECTOR('',#11378,1.);
#3298=VECTOR('',#11379,1.);
#3299=VECTOR('',#11392,0.2);
#3300=VECTOR('',#11405,0.325);
#3301=VECTOR('',#11410,0.35);
#3302=VECTOR('',#11415,0.335);
#3303=VECTOR('',#11424,0.21);
#3304=VECTOR('',#11429,0.2);
#3305=VECTOR('',#11432,0.18);
#3735=CIRCLE('',#9360,0.2);
#3736=CIRCLE('',#9361,0.16);
#3737=CIRCLE('',#9363,0.2);
#3738=CIRCLE('',#9366,0.3);
#3739=CIRCLE('',#9368,0.35);
#3740=CIRCLE('',#9370,0.35);
#3741=CIRCLE('',#9372,0.32);
#3742=CIRCLE('',#9374,0.22);
#3743=CIRCLE('',#9376,0.1954);
#3744=CIRCLE('',#9378,0.1954);
#4323=VERTEX_POINT('',#14195);
#4324=VERTEX_POINT('',#14196);
#4325=VERTEX_POINT('',#14198);
#4326=VERTEX_POINT('',#14200);
#4327=VERTEX_POINT('',#14204);
#4328=VERTEX_POINT('',#14206);
#4329=VERTEX_POINT('',#14210);
#4330=VERTEX_POINT('',#14212);
#4331=VERTEX_POINT('',#14216);
#4332=VERTEX_POINT('',#14218);
#4333=VERTEX_POINT('',#14222);
#4334=VERTEX_POINT('',#14224);
#4335=VERTEX_POINT('',#14233);
#4336=VERTEX_POINT('',#14235);
#4337=VERTEX_POINT('',#14238);
#4338=VERTEX_POINT('',#14243);
#4339=VERTEX_POINT('',#14246);
#4340=VERTEX_POINT('',#14250);
#4341=VERTEX_POINT('',#14254);
#4342=VERTEX_POINT('',#14258);
#4343=VERTEX_POINT('',#14261);
#4344=VERTEX_POINT('',#14265);
#5229=EDGE_CURVE('',#4323,#4324,#2651,.T.);
#5230=EDGE_CURVE('',#4324,#4325,#2652,.T.);
#5231=EDGE_CURVE('',#4325,#4326,#2653,.T.);
#5232=EDGE_CURVE('',#4323,#4326,#2654,.T.);
#5233=EDGE_CURVE('',#4324,#4327,#2655,.T.);
#5234=EDGE_CURVE('',#4327,#4328,#2656,.T.);
#5235=EDGE_CURVE('',#4328,#4325,#2657,.T.);
#5236=EDGE_CURVE('',#4327,#4329,#2658,.T.);
#5237=EDGE_CURVE('',#4329,#4330,#2659,.T.);
#5238=EDGE_CURVE('',#4330,#4328,#2660,.T.);
#5239=EDGE_CURVE('',#4329,#4331,#2661,.T.);
#5240=EDGE_CURVE('',#4331,#4332,#2662,.T.);
#5241=EDGE_CURVE('',#4332,#4330,#2663,.T.);
#5242=EDGE_CURVE('',#4331,#4333,#2664,.T.);
#5243=EDGE_CURVE('',#4333,#4334,#2665,.T.);
#5244=EDGE_CURVE('',#4334,#4332,#2666,.T.);
#5245=EDGE_CURVE('',#4333,#4323,#2667,.T.);
#5246=EDGE_CURVE('',#4326,#4334,#2668,.T.);
#5247=EDGE_CURVE('',#4335,#4335,#3735,.T.);
#5248=EDGE_CURVE('',#4336,#4336,#3736,.T.);
#5249=EDGE_CURVE('',#4335,#4337,#2669,.T.);
#5250=EDGE_CURVE('',#4337,#4337,#3737,.T.);
#5251=EDGE_CURVE('',#4338,#4338,#3738,.T.);
#5252=EDGE_CURVE('',#4339,#4339,#3739,.T.);
#5253=EDGE_CURVE('',#4339,#4338,#2670,.T.);
#5254=EDGE_CURVE('',#4340,#4340,#3740,.T.);
#5255=EDGE_CURVE('',#4340,#4339,#2671,.T.);
#5256=EDGE_CURVE('',#4341,#4341,#3741,.T.);
#5257=EDGE_CURVE('',#4341,#4340,#2672,.T.);
#5258=EDGE_CURVE('',#4342,#4342,#3742,.T.);
#5259=EDGE_CURVE('',#4343,#4343,#3743,.F.);
#5260=EDGE_CURVE('',#4343,#4342,#2673,.T.);
#5261=EDGE_CURVE('',#4344,#4344,#3744,.F.);
#5262=EDGE_CURVE('',#4344,#4343,#2674,.T.);
#5263=EDGE_CURVE('',#4336,#4344,#2675,.T.);
#6937=ORIENTED_EDGE('',*,*,#5229,.T.);
#6938=ORIENTED_EDGE('',*,*,#5230,.T.);
#6939=ORIENTED_EDGE('',*,*,#5231,.T.);
#6940=ORIENTED_EDGE('',*,*,#5232,.F.);
#6941=ORIENTED_EDGE('',*,*,#5233,.T.);
#6942=ORIENTED_EDGE('',*,*,#5234,.T.);
#6943=ORIENTED_EDGE('',*,*,#5235,.T.);
#6944=ORIENTED_EDGE('',*,*,#5230,.F.);
#6945=ORIENTED_EDGE('',*,*,#5236,.T.);
#6946=ORIENTED_EDGE('',*,*,#5237,.T.);
#6947=ORIENTED_EDGE('',*,*,#5238,.T.);
#6948=ORIENTED_EDGE('',*,*,#5234,.F.);
#6949=ORIENTED_EDGE('',*,*,#5239,.T.);
#6950=ORIENTED_EDGE('',*,*,#5240,.T.);
#6951=ORIENTED_EDGE('',*,*,#5241,.T.);
#6952=ORIENTED_EDGE('',*,*,#5237,.F.);
#6953=ORIENTED_EDGE('',*,*,#5242,.T.);
#6954=ORIENTED_EDGE('',*,*,#5243,.T.);
#6955=ORIENTED_EDGE('',*,*,#5244,.T.);
#6956=ORIENTED_EDGE('',*,*,#5240,.F.);
#6957=ORIENTED_EDGE('',*,*,#5245,.T.);
#6958=ORIENTED_EDGE('',*,*,#5232,.T.);
#6959=ORIENTED_EDGE('',*,*,#5246,.T.);
#6960=ORIENTED_EDGE('',*,*,#5243,.F.);
#6961=ORIENTED_EDGE('',*,*,#5245,.F.);
#6962=ORIENTED_EDGE('',*,*,#5242,.F.);
#6963=ORIENTED_EDGE('',*,*,#5239,.F.);
#6964=ORIENTED_EDGE('',*,*,#5236,.F.);
#6965=ORIENTED_EDGE('',*,*,#5233,.F.);
#6966=ORIENTED_EDGE('',*,*,#5229,.F.);
#6967=ORIENTED_EDGE('',*,*,#5246,.F.);
#6968=ORIENTED_EDGE('',*,*,#5231,.F.);
#6969=ORIENTED_EDGE('',*,*,#5235,.F.);
#6970=ORIENTED_EDGE('',*,*,#5238,.F.);
#6971=ORIENTED_EDGE('',*,*,#5241,.F.);
#6972=ORIENTED_EDGE('',*,*,#5244,.F.);
#6973=ORIENTED_EDGE('',*,*,#5247,.T.);
#6974=ORIENTED_EDGE('',*,*,#5248,.T.);
#6975=ORIENTED_EDGE('',*,*,#5247,.F.);
#6976=ORIENTED_EDGE('',*,*,#5249,.T.);
#6977=ORIENTED_EDGE('',*,*,#5250,.T.);
#6978=ORIENTED_EDGE('',*,*,#5249,.F.);
#6979=ORIENTED_EDGE('',*,*,#5250,.F.);
#6980=ORIENTED_EDGE('',*,*,#5251,.F.);
#6981=ORIENTED_EDGE('',*,*,#5252,.F.);
#6982=ORIENTED_EDGE('',*,*,#5253,.T.);
#6983=ORIENTED_EDGE('',*,*,#5251,.T.);
#6984=ORIENTED_EDGE('',*,*,#5253,.F.);
#6985=ORIENTED_EDGE('',*,*,#5254,.F.);
#6986=ORIENTED_EDGE('',*,*,#5255,.T.);
#6987=ORIENTED_EDGE('',*,*,#5252,.T.);
#6988=ORIENTED_EDGE('',*,*,#5255,.F.);
#6989=ORIENTED_EDGE('',*,*,#5256,.F.);
#6990=ORIENTED_EDGE('',*,*,#5257,.T.);
#6991=ORIENTED_EDGE('',*,*,#5254,.T.);
#6992=ORIENTED_EDGE('',*,*,#5257,.F.);
#6993=ORIENTED_EDGE('',*,*,#5256,.T.);
#6994=ORIENTED_EDGE('',*,*,#5258,.F.);
#6995=ORIENTED_EDGE('',*,*,#5259,.F.);
#6996=ORIENTED_EDGE('',*,*,#5260,.T.);
#6997=ORIENTED_EDGE('',*,*,#5258,.T.);
#6998=ORIENTED_EDGE('',*,*,#5260,.F.);
#6999=ORIENTED_EDGE('',*,*,#5261,.F.);
#7000=ORIENTED_EDGE('',*,*,#5262,.T.);
#7001=ORIENTED_EDGE('',*,*,#5259,.T.);
#7002=ORIENTED_EDGE('',*,*,#5262,.F.);
#7003=ORIENTED_EDGE('',*,*,#5248,.F.);
#7004=ORIENTED_EDGE('',*,*,#5263,.T.);
#7005=ORIENTED_EDGE('',*,*,#5261,.T.);
#7006=ORIENTED_EDGE('',*,*,#5263,.F.);
#7709=CYLINDRICAL_SURFACE('',#9362,0.2);
#7710=CYLINDRICAL_SURFACE('',#9369,0.35);
#7711=CYLINDRICAL_SURFACE('',#9377,0.1954);
#8066=ADVANCED_FACE('',(#1394),#972,.F.);
#8067=ADVANCED_FACE('',(#1395),#973,.F.);
#8068=ADVANCED_FACE('',(#1396),#974,.F.);
#8069=ADVANCED_FACE('',(#1397),#975,.F.);
#8070=ADVANCED_FACE('',(#1398),#976,.F.);
#8071=ADVANCED_FACE('',(#1399),#977,.F.);
#8072=ADVANCED_FACE('',(#1400),#978,.F.);
#8073=ADVANCED_FACE('',(#1401),#979,.F.);
#8074=ADVANCED_FACE('',(#1402,#740),#980,.T.);
#8075=ADVANCED_FACE('',(#1403),#7709,.T.);
#8076=ADVANCED_FACE('',(#1404),#981,.F.);
#8077=ADVANCED_FACE('',(#1405),#982,.T.);
#8078=ADVANCED_FACE('',(#1406),#413,.T.);
#8079=ADVANCED_FACE('',(#1407),#7710,.T.);
#8080=ADVANCED_FACE('',(#1408),#414,.T.);
#8081=ADVANCED_FACE('',(#1409,#741),#983,.T.);
#8082=ADVANCED_FACE('',(#1410),#415,.T.);
#8083=ADVANCED_FACE('',(#1411),#7711,.T.);
#8084=ADVANCED_FACE('',(#1412),#416,.T.);
#8277=CLOSED_SHELL('',(#8066,#8067,#8068,#8069,#8070,#8071,#8072,#8073));
#8278=CLOSED_SHELL('',(#8074,#8075,#8076,#8077,#8078,#8079,#8080,#8081,
#8082,#8083,#8084));
#9350=AXIS2_PLACEMENT_3D('',#14193,#11348,#11349);
#9351=AXIS2_PLACEMENT_3D('',#14194,#11350,#11351);
#9352=AXIS2_PLACEMENT_3D('',#14203,#11356,#11357);
#9353=AXIS2_PLACEMENT_3D('',#14209,#11361,#11362);
#9354=AXIS2_PLACEMENT_3D('',#14215,#11366,#11367);
#9355=AXIS2_PLACEMENT_3D('',#14221,#11371,#11372);
#9356=AXIS2_PLACEMENT_3D('',#14227,#11376,#11377);
#9357=AXIS2_PLACEMENT_3D('',#14230,#11380,#11381);
#9358=AXIS2_PLACEMENT_3D('',#14231,#11382,#11383);
#9359=AXIS2_PLACEMENT_3D('',#14232,#11384,#11385);
#9360=AXIS2_PLACEMENT_3D('',#14234,#11386,#11387);
#9361=AXIS2_PLACEMENT_3D('',#14236,#11388,#11389);
#9362=AXIS2_PLACEMENT_3D('',#14237,#11390,#11391);
#9363=AXIS2_PLACEMENT_3D('',#14240,#11393,#11394);
#9364=AXIS2_PLACEMENT_3D('',#14241,#11395,#11396);
#9365=AXIS2_PLACEMENT_3D('',#14242,#11397,#11398);
#9366=AXIS2_PLACEMENT_3D('',#14244,#11399,#11400);
#9367=AXIS2_PLACEMENT_3D('',#14245,#11401,#11402);
#9368=AXIS2_PLACEMENT_3D('',#14247,#11403,#11404);
#9369=AXIS2_PLACEMENT_3D('',#14249,#11406,#11407);
#9370=AXIS2_PLACEMENT_3D('',#14251,#11408,#11409);
#9371=AXIS2_PLACEMENT_3D('',#14253,#11411,#11412);
#9372=AXIS2_PLACEMENT_3D('',#14255,#11413,#11414);
#9373=AXIS2_PLACEMENT_3D('',#14257,#11416,#11417);
#9374=AXIS2_PLACEMENT_3D('',#14259,#11418,#11419);
#9375=AXIS2_PLACEMENT_3D('',#14260,#11420,#11421);
#9376=AXIS2_PLACEMENT_3D('',#14262,#11422,#11423);
#9377=AXIS2_PLACEMENT_3D('',#14264,#11425,#11426);
#9378=AXIS2_PLACEMENT_3D('',#14266,#11427,#11428);
#9379=AXIS2_PLACEMENT_3D('',#14268,#11430,#11431);
#11348=DIRECTION('axis',(0.,0.,1.));
#11349=DIRECTION('refdir',(1.,0.,0.));
#11350=DIRECTION('center_axis',(0.866025403784439,0.,-0.5));
#11351=DIRECTION('ref_axis',(0.5,0.,0.866025403784439));
#11352=DIRECTION('',(-0.5,0.,-0.866025403784439));
#11353=DIRECTION('',(0.,-1.,0.));
#11354=DIRECTION('',(0.5,0.,0.866025403784439));
#11355=DIRECTION('',(0.,-1.,0.));
#11356=DIRECTION('center_axis',(1.60246890531964E-16,0.,-1.));
#11357=DIRECTION('ref_axis',(1.,0.,1.60246890531964E-16));
#11358=DIRECTION('',(-1.,0.,-1.60246890531964E-16));
#11359=DIRECTION('',(0.,-1.,0.));
#11360=DIRECTION('',(1.,0.,1.60246890531964E-16));
#11361=DIRECTION('center_axis',(-0.866025403784439,0.,-0.5));
#11362=DIRECTION('ref_axis',(0.5,0.,-0.866025403784439));
#11363=DIRECTION('',(-0.5,0.,0.866025403784439));
#11364=DIRECTION('',(0.,-1.,0.));
#11365=DIRECTION('',(0.5,0.,-0.866025403784439));
#11366=DIRECTION('center_axis',(-0.866025403784439,0.,0.5));
#11367=DIRECTION('ref_axis',(-0.5,0.,-0.866025403784439));
#11368=DIRECTION('',(0.5,0.,0.866025403784439));
#11369=DIRECTION('',(0.,-1.,0.));
#11370=DIRECTION('',(-0.5,0.,-0.866025403784439));
#11371=DIRECTION('center_axis',(-1.60246890531964E-16,0.,1.));
#11372=DIRECTION('ref_axis',(-1.,0.,-1.60246890531964E-16));
#11373=DIRECTION('',(1.,0.,1.60246890531964E-16));
#11374=DIRECTION('',(0.,-1.,0.));
#11375=DIRECTION('',(-1.,0.,-1.60246890531964E-16));
#11376=DIRECTION('center_axis',(0.866025403784439,0.,0.5));
#11377=DIRECTION('ref_axis',(-0.5,0.,0.866025403784439));
#11378=DIRECTION('',(0.5,0.,-0.866025403784439));
#11379=DIRECTION('',(-0.5,0.,0.866025403784439));
#11380=DIRECTION('center_axis',(0.,1.,0.));
#11381=DIRECTION('ref_axis',(1.,0.,0.));
#11382=DIRECTION('center_axis',(0.,-1.,0.));
#11383=DIRECTION('ref_axis',(0.,0.,-1.));
#11384=DIRECTION('center_axis',(0.,1.,0.));
#11385=DIRECTION('ref_axis',(1.,0.,0.));
#11386=DIRECTION('center_axis',(0.,1.,0.));
#11387=DIRECTION('ref_axis',(1.,0.,0.));
#11388=DIRECTION('center_axis',(0.,-1.,0.));
#11389=DIRECTION('ref_axis',(1.,0.,0.));
#11390=DIRECTION('center_axis',(0.,1.,0.));
#11391=DIRECTION('ref_axis',(1.,0.,0.));
#11392=DIRECTION('',(0.,-1.,0.));
#11393=DIRECTION('center_axis',(0.,1.,0.));
#11394=DIRECTION('ref_axis',(1.,0.,0.));
#11395=DIRECTION('center_axis',(0.,1.,0.));
#11396=DIRECTION('ref_axis',(1.,0.,0.));
#11397=DIRECTION('center_axis',(0.,1.,0.));
#11398=DIRECTION('ref_axis',(0.,0.,1.));
#11399=DIRECTION('center_axis',(0.,-1.,0.));
#11400=DIRECTION('ref_axis',(1.,0.,0.));
#11401=DIRECTION('center_axis',(0.,-1.,0.));
#11402=DIRECTION('ref_axis',(1.,0.,0.));
#11403=DIRECTION('center_axis',(0.,-1.,0.));
#11404=DIRECTION('ref_axis',(1.,0.,0.));
#11405=DIRECTION('',(0.707106781186547,0.707106781186548,8.65956056235493E-17));
#11406=DIRECTION('center_axis',(0.,-1.,0.));
#11407=DIRECTION('ref_axis',(1.,0.,0.));
#11408=DIRECTION('center_axis',(0.,-1.,0.));
#11409=DIRECTION('ref_axis',(1.,0.,0.));
#11410=DIRECTION('',(0.,1.,0.));
#11411=DIRECTION('center_axis',(0.,1.,0.));
#11412=DIRECTION('ref_axis',(1.,0.,0.));
#11413=DIRECTION('center_axis',(0.,-1.,0.));
#11414=DIRECTION('ref_axis',(1.,0.,0.));
#11415=DIRECTION('',(-0.707106781186547,0.707106781186548,-8.65956056235493E-17));
#11416=DIRECTION('center_axis',(0.,-1.,0.));
#11417=DIRECTION('ref_axis',(0.,0.,-1.));
#11418=DIRECTION('center_axis',(0.,-1.,0.));
#11419=DIRECTION('ref_axis',(1.,0.,0.));
#11420=DIRECTION('center_axis',(0.,1.,0.));
#11421=DIRECTION('ref_axis',(1.,0.,0.));
#11422=DIRECTION('center_axis',(0.,1.,0.));
#11423=DIRECTION('ref_axis',(1.,0.,0.));
#11424=DIRECTION('',(-0.447213595499958,0.894427190999916,-5.47678698264203E-17));
#11425=DIRECTION('center_axis',(0.,-1.,0.));
#11426=DIRECTION('ref_axis',(1.,0.,0.));
#11427=DIRECTION('center_axis',(0.,1.,0.));
#11428=DIRECTION('ref_axis',(1.,0.,0.));
#11429=DIRECTION('',(0.,1.,0.));
#11430=DIRECTION('center_axis',(0.,1.,0.));
#11431=DIRECTION('ref_axis',(1.,0.,0.));
#11432=DIRECTION('',(-0.707106781186547,0.707106781186548,-8.65956056235493E-17));
#14193=CARTESIAN_POINT('',(0.,0.,0.));
#14194=CARTESIAN_POINT('Origin',(0.0866025403784439,-0.4,-0.15));
#14195=CARTESIAN_POINT('',(0.173205080756888,-0.4,0.));
#14196=CARTESIAN_POINT('',(0.0866025403784439,-0.4,-0.15));
#14197=CARTESIAN_POINT('',(0.173205080756888,-0.4,0.));
#14198=CARTESIAN_POINT('',(0.0866025403784439,-0.64,-0.15));
#14199=CARTESIAN_POINT('',(0.0866025403784439,-0.4,-0.15));
#14200=CARTESIAN_POINT('',(0.173205080756888,-0.64,0.));
#14201=CARTESIAN_POINT('',(0.173205080756888,-0.64,0.));
#14202=CARTESIAN_POINT('',(0.173205080756888,-0.4,0.));
#14203=CARTESIAN_POINT('Origin',(-0.0866025403784438,-0.4,-0.15));
#14204=CARTESIAN_POINT('',(-0.0866025403784438,-0.4,-0.15));
#14205=CARTESIAN_POINT('',(0.0866025403784439,-0.4,-0.15));
#14206=CARTESIAN_POINT('',(-0.0866025403784438,-0.64,-0.15));
#14207=CARTESIAN_POINT('',(-0.0866025403784438,-0.4,-0.15));
#14208=CARTESIAN_POINT('',(0.0866025403784439,-0.64,-0.15));
#14209=CARTESIAN_POINT('Origin',(-0.173205080756888,-0.4,-2.77555756156289E-17));
#14210=CARTESIAN_POINT('',(-0.173205080756888,-0.4,-2.12115047744981E-17));
#14211=CARTESIAN_POINT('',(-0.0866025403784438,-0.4,-0.15));
#14212=CARTESIAN_POINT('',(-0.173205080756888,-0.64,-2.77555756156289E-17));
#14213=CARTESIAN_POINT('',(-0.173205080756888,-0.4,-2.12115047744981E-17));
#14214=CARTESIAN_POINT('',(-0.0866025403784438,-0.64,-0.15));
#14215=CARTESIAN_POINT('Origin',(-0.0866025403784439,-0.4,0.15));
#14216=CARTESIAN_POINT('',(-0.0866025403784439,-0.4,0.15));
#14217=CARTESIAN_POINT('',(-0.173205080756888,-0.4,-2.12115047744981E-17));
#14218=CARTESIAN_POINT('',(-0.0866025403784439,-0.64,0.15));
#14219=CARTESIAN_POINT('',(-0.0866025403784439,-0.4,0.15));
#14220=CARTESIAN_POINT('',(-0.173205080756888,-0.64,-2.12115047744981E-17));
#14221=CARTESIAN_POINT('Origin',(0.0866025403784439,-0.4,0.15));
#14222=CARTESIAN_POINT('',(0.0866025403784439,-0.4,0.15));
#14223=CARTESIAN_POINT('',(-0.0866025403784439,-0.4,0.15));
#14224=CARTESIAN_POINT('',(0.0866025403784439,-0.64,0.15));
#14225=CARTESIAN_POINT('',(0.0866025403784439,-0.4,0.15));
#14226=CARTESIAN_POINT('',(-0.0866025403784439,-0.64,0.15));
#14227=CARTESIAN_POINT('Origin',(0.173205080756888,-0.4,0.));
#14228=CARTESIAN_POINT('',(0.0866025403784439,-0.4,0.15));
#14229=CARTESIAN_POINT('',(0.0866025403784439,-0.64,0.15));
#14230=CARTESIAN_POINT('Origin',(0.,-0.4,-2.77555756156289E-17));
#14231=CARTESIAN_POINT('Origin',(0.,-0.64,-2.77555756156289E-17));
#14232=CARTESIAN_POINT('Origin',(0.,-1.6,0.));
#14233=CARTESIAN_POINT('',(-0.2,-1.6,2.44929359829471E-17));
#14234=CARTESIAN_POINT('Origin',(0.,-1.6,0.));
#14235=CARTESIAN_POINT('',(-0.16,-1.6,-1.95943487863577E-17));
#14236=CARTESIAN_POINT('Origin',(0.,-1.6,0.));
#14237=CARTESIAN_POINT('Origin',(0.,-3.,0.));
#14238=CARTESIAN_POINT('',(-0.2,-3.,2.44929359829471E-17));
#14239=CARTESIAN_POINT('',(-0.2,-3.,2.44929359829471E-17));
#14240=CARTESIAN_POINT('Origin',(0.,-3.,0.));
#14241=CARTESIAN_POINT('Origin',(0.,-3.,0.));
#14242=CARTESIAN_POINT('Origin',(0.3,0.4,0.));
#14243=CARTESIAN_POINT('',(-0.3,0.4,-3.67394039744206E-17));
#14244=CARTESIAN_POINT('Origin',(0.,0.4,0.));
#14245=CARTESIAN_POINT('Origin',(0.,0.375,0.));
#14246=CARTESIAN_POINT('',(-0.35,0.35,-4.28626379701573E-17));
#14247=CARTESIAN_POINT('Origin',(0.,0.35,0.));
#14248=CARTESIAN_POINT('',(-0.325,0.375,-3.9801020972289E-17));
#14249=CARTESIAN_POINT('Origin',(0.,0.19,0.));
#14250=CARTESIAN_POINT('',(-0.35,0.03,-4.28626379701574E-17));
#14251=CARTESIAN_POINT('Origin',(0.,0.03,0.));
#14252=CARTESIAN_POINT('',(-0.35,0.19,-4.28626379701574E-17));
#14253=CARTESIAN_POINT('Origin',(0.,0.0149999999999999,0.));
#14254=CARTESIAN_POINT('',(-0.32,-3.29597460435593E-17,-3.91886975727153E-17));
#14255=CARTESIAN_POINT('Origin',(0.,0.,0.));
#14256=CARTESIAN_POINT('',(-0.335,0.0149999999999999,-4.10256677714363E-17));
#14257=CARTESIAN_POINT('Origin',(0.22,0.,0.));
#14258=CARTESIAN_POINT('',(-0.22,-6.93889390390723E-18,-2.69422295812418E-17));
#14259=CARTESIAN_POINT('Origin',(0.,0.,0.));
#14260=CARTESIAN_POINT('Origin',(0.,-0.02,0.));
#14261=CARTESIAN_POINT('',(-0.1954,-0.0492,2.39295984553393E-17));
#14262=CARTESIAN_POINT('Origin',(0.,-0.0492,0.));
#14263=CARTESIAN_POINT('',(-0.21,-0.02,-2.57175827820944E-17));
#14264=CARTESIAN_POINT('Origin',(0.,-0.8,0.));
#14265=CARTESIAN_POINT('',(-0.1954,-1.5646,2.39295984553393E-17));
#14266=CARTESIAN_POINT('Origin',(0.,-1.5646,0.));
#14267=CARTESIAN_POINT('',(-0.1954,-0.8,-2.39295984553393E-17));
#14268=CARTESIAN_POINT('Origin',(0.,-1.58,0.));
#14269=CARTESIAN_POINT('',(-0.18,-1.58,-2.20436423846524E-17));
#15140=UNCERTAINTY_MEASURE_WITH_UNIT(LENGTH_MEASURE(0.001),#15213,
'DISTANCE_ACCURACY_VALUE',
'Maximum model space distance between geometric entities at asserted c
onnectivities');
#15162=UNCERTAINTY_MEASURE_WITH_UNIT(LENGTH_MEASURE(0.001),#15213,
'DISTANCE_ACCURACY_VALUE',
'Maximum model space distance between geometric entities at asserted c
onnectivities');
#15190=(
GEOMETRIC_REPRESENTATION_CONTEXT(3)
GLOBAL_UNCERTAINTY_ASSIGNED_CONTEXT((#15140))
GLOBAL_UNIT_ASSIGNED_CONTEXT((#15213,#15215,#15216))
REPRESENTATION_CONTEXT('','3D')
);
#15212=(
GEOMETRIC_REPRESENTATION_CONTEXT(3)
GLOBAL_UNCERTAINTY_ASSIGNED_CONTEXT((#15162))
GLOBAL_UNIT_ASSIGNED_CONTEXT((#15213,#15215,#15216))
REPRESENTATION_CONTEXT('','3D')
);
#15213=(
LENGTH_UNIT()
NAMED_UNIT(*)
SI_UNIT(.CENTI.,.METRE.)
);
#15215=(
NAMED_UNIT(*)
PLANE_ANGLE_UNIT()
SI_UNIT($,.RADIAN.)
);
#15216=(
NAMED_UNIT(*)
SI_UNIT($,.STERADIAN.)
SOLID_ANGLE_UNIT()
);
#15244=SHAPE_DEFINITION_REPRESENTATION(#15300,#15428);
#15300=PRODUCT_DEFINITION_SHAPE('',$,#15478);
#15428=SHAPE_REPRESENTATION('',(#9350),#15190);
#15450=PRODUCT_DEFINITION_CONTEXT('part definition',#15599,'design');
#15478=PRODUCT_DEFINITION('M4x30 stop screw','M4x30 stop screw',#15527,
#15450);
#15527=PRODUCT_DEFINITION_FORMATION('',$,#15628);
#15599=APPLICATION_CONTEXT(
'Core Data for Automotive Mechanical Design Process');
#15600=PRODUCT_CONTEXT('part definition',#15599,'mechanical');
#15628=PRODUCT('M4x30 stop screw','M4x30 stop screw','M4x30 stop screw',
(#15600));
#15720=COLOUR_RGB('Black',0.12,0.14,0.17);
#15721=FILL_AREA_STYLE_COLOUR('',#15720);
#15722=FILL_AREA_STYLE('',(#15721));
#15723=SURFACE_STYLE_FILL_AREA(#15722);
#15724=SURFACE_SIDE_STYLE('',(#15723));
#15725=SURFACE_STYLE_USAGE(.BOTH.,#15724);
#15726=PRESENTATION_STYLE_ASSIGNMENT((#15725));
ENDSEC;
END-ISO-10303-21;
